ISO-10303-21;
HEADER;
/* Generated by software containing ST-Developer
 * from STEP Tools, Inc. (www.steptools.com) 
 */

FILE_DESCRIPTION(
/* description */ ('Double-row support with tensioned shaft'),
/* implementation_level */ '2;1');

FILE_NAME(
/* name */ 'Bonded foot pad (2).step',
/* time_stamp */ '2026-10-27T10:50:35-07:00',
/* author */ (''),
/* organization */ (''),
/* preprocessor_version */ 'ST-DEVELOPER v20.2',
/* originating_system */ 'Autodesk Translation Framework v15.17.0.0',
/* authorisation */ '');

FILE_SCHEMA (('AUTOMOTIVE_DESIGN { 1 0 10303 214 3 1 1 }'));
ENDSEC;

DATA;
#10=MECHANICAL_DESIGN_GEOMETRIC_PRESENTATION_REPRESENTATION('',(#482),#11559);
#418=SHAPE_REPRESENTATION_RELATIONSHIP('SRR','None',#11726,#450);
#450=ADVANCED_BREP_SHAPE_REPRESENTATION('',(#515),#11528);
#482=STYLED_ITEM('',(#11960),#515);
#515=MANIFOLD_SOLID_BREP('Body1',#6327);
#697=PLANE('',#6773);
#698=PLANE('',#6774);
#699=PLANE('',#6775);
#700=PLANE('',#6776);
#701=PLANE('',#6777);
#702=PLANE('',#6778);
#947=FACE_OUTER_BOUND('',#1315,.T.);
#948=FACE_OUTER_BOUND('',#1316,.T.);
#949=FACE_OUTER_BOUND('',#1317,.T.);
#950=FACE_OUTER_BOUND('',#1318,.T.);
#951=FACE_OUTER_BOUND('',#1319,.T.);
#952=FACE_OUTER_BOUND('',#1320,.T.);
#1315=EDGE_LOOP('',(#4474,#4475,#4476,#4477));
#1316=EDGE_LOOP('',(#4478,#4479,#4480,#4481));
#1317=EDGE_LOOP('',(#4482,#4483,#4484,#4485));
#1318=EDGE_LOOP('',(#4486,#4487,#4488,#4489));
#1319=EDGE_LOOP('',(#4490,#4491,#4492,#4493));
#1320=EDGE_LOOP('',(#4494,#4495,#4496,#4497));
#1790=LINE('',#9393,#2337);
#1791=LINE('',#9395,#2338);
#1792=LINE('',#9397,#2339);
#1793=LINE('',#9398,#2340);
#1794=LINE('',#9401,#2341);
#1795=LINE('',#9403,#2342);
#1796=LINE('',#9404,#2343);
#1797=LINE('',#9407,#2344);
#1798=LINE('',#9409,#2345);
#1799=LINE('',#9410,#2346);
#1800=LINE('',#9412,#2347);
#1801=LINE('',#9413,#2348);
#2337=VECTOR('',#7541,1.);
#2338=VECTOR('',#7542,1.);
#2339=VECTOR('',#7543,1.);
#2340=VECTOR('',#7544,1.);
#2341=VECTOR('',#7547,1.);
#2342=VECTOR('',#7548,1.);
#2343=VECTOR('',#7549,1.);
#2344=VECTOR('',#7552,1.);
#2345=VECTOR('',#7553,1.);
#2346=VECTOR('',#7554,1.);
#2347=VECTOR('',#7557,1.);
#2348=VECTOR('',#7558,1.);
#3075=VERTEX_POINT('',#9391);
#3076=VERTEX_POINT('',#9392);
#3077=VERTEX_POINT('',#9394);
#3078=VERTEX_POINT('',#9396);
#3079=VERTEX_POINT('',#9400);
#3080=VERTEX_POINT('',#9402);
#3081=VERTEX_POINT('',#9406);
#3082=VERTEX_POINT('',#9408);
#3622=EDGE_CURVE('',#3075,#3076,#1790,.T.);
#3623=EDGE_CURVE('',#3076,#3077,#1791,.T.);
#3624=EDGE_CURVE('',#3078,#3077,#1792,.T.);
#3625=EDGE_CURVE('',#3075,#3078,#1793,.T.);
#3626=EDGE_CURVE('',#3079,#3075,#1794,.T.);
#3627=EDGE_CURVE('',#3080,#3078,#1795,.T.);
#3628=EDGE_CURVE('',#3079,#3080,#1796,.T.);
#3629=EDGE_CURVE('',#3081,#3079,#1797,.T.);
#3630=EDGE_CURVE('',#3082,#3080,#1798,.T.);
#3631=EDGE_CURVE('',#3081,#3082,#1799,.T.);
#3632=EDGE_CURVE('',#3076,#3081,#1800,.T.);
#3633=EDGE_CURVE('',#3077,#3082,#1801,.T.);
#4474=ORIENTED_EDGE('',*,*,#3622,.T.);
#4475=ORIENTED_EDGE('',*,*,#3623,.T.);
#4476=ORIENTED_EDGE('',*,*,#3624,.F.);
#4477=ORIENTED_EDGE('',*,*,#3625,.F.);
#4478=ORIENTED_EDGE('',*,*,#3626,.T.);
#4479=ORIENTED_EDGE('',*,*,#3625,.T.);
#4480=ORIENTED_EDGE('',*,*,#3627,.F.);
#4481=ORIENTED_EDGE('',*,*,#3628,.F.);
#4482=ORIENTED_EDGE('',*,*,#3629,.T.);
#4483=ORIENTED_EDGE('',*,*,#3628,.T.);
#4484=ORIENTED_EDGE('',*,*,#3630,.F.);
#4485=ORIENTED_EDGE('',*,*,#3631,.F.);
#4486=ORIENTED_EDGE('',*,*,#3632,.T.);
#4487=ORIENTED_EDGE('',*,*,#3631,.T.);
#4488=ORIENTED_EDGE('',*,*,#3633,.F.);
#4489=ORIENTED_EDGE('',*,*,#3623,.F.);
#4490=ORIENTED_EDGE('',*,*,#3633,.T.);
#4491=ORIENTED_EDGE('',*,*,#3630,.T.);
#4492=ORIENTED_EDGE('',*,*,#3627,.T.);
#4493=ORIENTED_EDGE('',*,*,#3624,.T.);
#4494=ORIENTED_EDGE('',*,*,#3632,.F.);
#4495=ORIENTED_EDGE('',*,*,#3622,.F.);
#4496=ORIENTED_EDGE('',*,*,#3626,.F.);
#4497=ORIENTED_EDGE('',*,*,#3629,.F.);
#6010=ADVANCED_FACE('',(#947),#697,.T.);
#6011=ADVANCED_FACE('',(#948),#698,.T.);
#6012=ADVANCED_FACE('',(#949),#699,.T.);
#6013=ADVANCED_FACE('',(#950),#700,.T.);
#6014=ADVANCED_FACE('',(#951),#701,.T.);
#6015=ADVANCED_FACE('',(#952),#702,.F.);
#6327=CLOSED_SHELL('',(#6010,#6011,#6012,#6013,#6014,#6015));
#6772=AXIS2_PLACEMENT_3D('',#9389,#7537,#7538);
#6773=AXIS2_PLACEMENT_3D('',#9390,#7539,#7540);
#6774=AXIS2_PLACEMENT_3D('',#9399,#7545,#7546);
#6775=AXIS2_PLACEMENT_3D('',#9405,#7550,#7551);
#6776=AXIS2_PLACEMENT_3D('',#9411,#7555,#7556);
#6777=AXIS2_PLACEMENT_3D('',#9414,#7559,#7560);
#6778=AXIS2_PLACEMENT_3D('',#9415,#7561,#7562);
#7537=DIRECTION('axis',(0.,0.,1.));
#7538=DIRECTION('refdir',(1.,0.,0.));
#7539=DIRECTION('center_axis',(0.,1.,0.));
#7540=DIRECTION('ref_axis',(-1.,0.,0.));
#7541=DIRECTION('',(-1.,0.,0.));
#7542=DIRECTION('',(0.,0.,1.));
#7543=DIRECTION('',(-1.,0.,0.));
#7544=DIRECTION('',(0.,0.,1.));
#7545=DIRECTION('center_axis',(1.,0.,0.));
#7546=DIRECTION('ref_axis',(0.,1.,0.));
#7547=DIRECTION('',(0.,1.,0.));
#7548=DIRECTION('',(0.,1.,0.));
#7549=DIRECTION('',(0.,0.,1.));
#7550=DIRECTION('center_axis',(0.,-1.,0.));
#7551=DIRECTION('ref_axis',(1.,0.,0.));
#7552=DIRECTION('',(1.,0.,0.));
#7553=DIRECTION('',(1.,0.,0.));
#7554=DIRECTION('',(0.,0.,1.));
#7555=DIRECTION('center_axis',(-1.,0.,0.));
#7556=DIRECTION('ref_axis',(0.,-1.,0.));
#7557=DIRECTION('',(0.,-1.,0.));
#7558=DIRECTION('',(0.,-1.,0.));
#7559=DIRECTION('center_axis',(0.,0.,1.));
#7560=DIRECTION('ref_axis',(1.,0.,0.));
#7561=DIRECTION('center_axis',(0.,0.,1.));
#7562=DIRECTION('ref_axis',(1.,0.,0.));
#9389=CARTESIAN_POINT('',(0.,0.,0.));
#9390=CARTESIAN_POINT('Origin',(10.,14.,-0.4));
#9391=CARTESIAN_POINT('',(10.,14.,-0.4));
#9392=CARTESIAN_POINT('',(-10.,14.,-0.4));
#9393=CARTESIAN_POINT('',(10.,14.,-0.4));
#9394=CARTESIAN_POINT('',(-10.,14.,0.));
#9395=CARTESIAN_POINT('',(-10.,14.,-0.4));
#9396=CARTESIAN_POINT('',(10.,14.,0.));
#9397=CARTESIAN_POINT('',(10.,14.,0.));
#9398=CARTESIAN_POINT('',(10.,14.,-0.4));
#9399=CARTESIAN_POINT('Origin',(10.,12.,-0.4));
#9400=CARTESIAN_POINT('',(10.,12.,-0.4));
#9401=CARTESIAN_POINT('',(10.,12.,-0.4));
#9402=CARTESIAN_POINT('',(10.,12.,0.));
#9403=CARTESIAN_POINT('',(10.,12.,0.));
#9404=CARTESIAN_POINT('',(10.,12.,-0.4));
#9405=CARTESIAN_POINT('Origin',(-10.,12.,-0.4));
#9406=CARTESIAN_POINT('',(-10.,12.,-0.4));
#9407=CARTESIAN_POINT('',(-10.,12.,-0.4));
#9408=CARTESIAN_POINT('',(-10.,12.,0.));
#9409=CARTESIAN_POINT('',(-10.,12.,0.));
#9410=CARTESIAN_POINT('',(-10.,12.,-0.4));
#9411=CARTESIAN_POINT('Origin',(-10.,14.,-0.4));
#9412=CARTESIAN_POINT('',(-10.,14.,-0.4));
#9413=CARTESIAN_POINT('',(-10.,14.,0.));
#9414=CARTESIAN_POINT('Origin',(0.,13.,0.));
#9415=CARTESIAN_POINT('Origin',(0.,13.,-0.4));
#11491=UNCERTAINTY_MEASURE_WITH_UNIT(LENGTH_MEASURE(0.001),#11560,
'DISTANCE_ACCURACY_VALUE',
'Maximum model space distance between geometric entities at asserted c
onnectivities');
#11522=UNCERTAINTY_MEASURE_WITH_UNIT(LENGTH_MEASURE(0.001),#11560,
'DISTANCE_ACCURACY_VALUE',
'Maximum model space distance between geometric entities at asserted c
onnectivities');
#11528=(
GEOMETRIC_REPRESENTATION_CONTEXT(3)
GLOBAL_UNCERTAINTY_ASSIGNED_CONTEXT((#11491))
GLOBAL_UNIT_ASSIGNED_CONTEXT((#11560,#11562,#11563))
REPRESENTATION_CONTEXT('','3D')
);
#11559=(
GEOMETRIC_REPRESENTATION_CONTEXT(3)
GLOBAL_UNCERTAINTY_ASSIGNED_CONTEXT((#11522))
GLOBAL_UNIT_ASSIGNED_CONTEXT((#11560,#11562,#11563))
REPRESENTATION_CONTEXT('','3D')
);
#11560=(
LENGTH_UNIT()
NAMED_UNIT(*)
SI_UNIT(.CENTI.,.METRE.)
);
#11562=(
NAMED_UNIT(*)
PLANE_ANGLE_UNIT()
SI_UNIT($,.RADIAN.)
);
#11563=(
NAMED_UNIT(*)
SI_UNIT($,.STERADIAN.)
SOLID_ANGLE_UNIT()
);
#11569=SHAPE_DEFINITION_REPRESENTATION(#11605,#11726);
#11605=PRODUCT_DEFINITION_SHAPE('',$,#11763);
#11726=SHAPE_REPRESENTATION('',(#6772),#11528);
#11757=PRODUCT_DEFINITION_CONTEXT('part definition',#11867,'design');
#11763=PRODUCT_DEFINITION('Bonded foot pad (2)','Bonded foot pad (2)',#11799,
#11757);
#11799=PRODUCT_DEFINITION_FORMATION('',$,#11874);
#11867=APPLICATION_CONTEXT(
'Core Data for Automotive Mechanical Design Process');
#11868=PRODUCT_CONTEXT('part definition',#11867,'mechanical');
#11874=PRODUCT('Bonded foot pad (2)','Bonded foot pad (2)',
'Bonded foot pad (2)',(#11868));
#11954=COLOUR_RGB('Sky Blue',0.24,0.69,0.87);
#11955=FILL_AREA_STYLE_COLOUR('',#11954);
#11956=FILL_AREA_STYLE('',(#11955));
#11957=SURFACE_STYLE_FILL_AREA(#11956);
#11958=SURFACE_SIDE_STYLE('',(#11957));
#11959=SURFACE_STYLE_USAGE(.BOTH.,#11958);
#11960=PRESENTATION_STYLE_ASSIGNMENT((#11959));
ENDSEC;
END-ISO-10303-21;
